ISO-10303-21;
HEADER;
/* Generated by software containing ST-Developer
 * from STEP Tools, Inc. (www.steptools.com) 
 */

FILE_DESCRIPTION(
/* description */ ('CAx-IF Rec.Pracs.---Representation and Presentation of Product Manufa
cturing Information (PMI)---4.0---2014-10-13'),
/* implementation_level */ '2;1');

FILE_NAME(
/* name */ 'Bearing Retainer 1.step',
/* time_stamp */ '2026-10-24T15:58:00-07:00',
/* author */ (''),
/* organization */ (''),
/* preprocessor_version */ 'ST-DEVELOPER v20.2',
/* originating_system */ 'Autodesk Translation Framework v15.17.0.0',
/* authorisation */ '');

FILE_SCHEMA (('AP242_MANAGED_MODEL_BASED_3D_ENGINEERING_MIM_LF { 1 0 10303 442 2 1 4 }'));
ENDSEC;

DATA;
#10=MECHANICAL_DESIGN_GEOMETRIC_PRESENTATION_REPRESENTATION('',(#135),#8944);
#105=CONICAL_SURFACE('',#5764,0.0043,0.785398163397448);
#106=CONICAL_SURFACE('',#5770,0.0046499998960644,0.785398163397448);
#117=SHAPE_REPRESENTATION_RELATIONSHIP('SRR','None',#9000,#126);
#126=ADVANCED_BREP_SHAPE_REPRESENTATION('',(#144),#8941);
#135=STYLED_ITEM('',(#9052),#144);
#144=MANIFOLD_SOLID_BREP('Body1',#5156);
#232=CYLINDRICAL_SURFACE('',#5760,0.0065);
#233=CYLINDRICAL_SURFACE('',#5766,0.00405);
#300=FACE_BOUND('',#891,.T.);
#301=FACE_BOUND('',#894,.T.);
#302=FACE_BOUND('',#898,.T.);
#559=FACE_OUTER_BOUND('',#890,.T.);
#560=FACE_OUTER_BOUND('',#892,.T.);
#561=FACE_OUTER_BOUND('',#893,.T.);
#562=FACE_OUTER_BOUND('',#895,.T.);
#563=FACE_OUTER_BOUND('',#896,.T.);
#564=FACE_OUTER_BOUND('',#897,.T.);
#565=FACE_OUTER_BOUND('',#899,.T.);
#890=EDGE_LOOP('',(#4653));
#891=EDGE_LOOP('',(#4654));
#892=EDGE_LOOP('',(#4655,#4656,#4657,#4658));
#893=EDGE_LOOP('',(#4659));
#894=EDGE_LOOP('',(#4660));
#895=EDGE_LOOP('',(#4661,#4662,#4663,#4664));
#896=EDGE_LOOP('',(#4665,#4666,#4667,#4668));
#897=EDGE_LOOP('',(#4669));
#898=EDGE_LOOP('',(#4670));
#899=EDGE_LOOP('',(#4671,#4672,#4673,#4674));
#1154=CIRCLE('',#5758,0.00650000000001);
#1155=CIRCLE('',#5759,0.00479999989272164);
#1156=CIRCLE('',#5761,0.00650000000001);
#1157=CIRCLE('',#5763,0.00455000000001);
#1158=CIRCLE('',#5765,0.00405000000001);
#1159=CIRCLE('',#5767,0.00405000000001);
#1160=CIRCLE('',#5769,0.00449999989942716);
#1617=LINE('',#8841,#2072);
#1618=LINE('',#8848,#2073);
#1619=LINE('',#8852,#2074);
#1620=LINE('',#8857,#2075);
#2072=VECTOR('',#7268,0.0065);
#2073=VECTOR('',#7277,0.0043);
#2074=VECTOR('',#7282,0.00405);
#2075=VECTOR('',#7289,0.0046499998960644);
#2540=VERTEX_POINT('',#8834);
#2541=VERTEX_POINT('',#8836);
#2542=VERTEX_POINT('',#8839);
#2543=VERTEX_POINT('',#8843);
#2544=VERTEX_POINT('',#8846);
#2545=VERTEX_POINT('',#8850);
#2546=VERTEX_POINT('',#8854);
#3247=EDGE_CURVE('',#2540,#2540,#1154,.T.);
#3248=EDGE_CURVE('',#2541,#2541,#1155,.T.);
#3249=EDGE_CURVE('',#2542,#2542,#1156,.T.);
#3250=EDGE_CURVE('',#2542,#2540,#1617,.T.);
#3251=EDGE_CURVE('',#2543,#2543,#1157,.T.);
#3252=EDGE_CURVE('',#2544,#2544,#1158,.T.);
#3253=EDGE_CURVE('',#2544,#2543,#1618,.T.);
#3254=EDGE_CURVE('',#2545,#2545,#1159,.T.);
#3255=EDGE_CURVE('',#2545,#2544,#1619,.T.);
#3256=EDGE_CURVE('',#2546,#2546,#1160,.T.);
#3257=EDGE_CURVE('',#2541,#2546,#1620,.T.);
#4653=ORIENTED_EDGE('',*,*,#3247,.F.);
#4654=ORIENTED_EDGE('',*,*,#3248,.T.);
#4655=ORIENTED_EDGE('',*,*,#3249,.F.);
#4656=ORIENTED_EDGE('',*,*,#3250,.T.);
#4657=ORIENTED_EDGE('',*,*,#3247,.T.);
#4658=ORIENTED_EDGE('',*,*,#3250,.F.);
#4659=ORIENTED_EDGE('',*,*,#3249,.T.);
#4660=ORIENTED_EDGE('',*,*,#3251,.F.);
#4661=ORIENTED_EDGE('',*,*,#3252,.F.);
#4662=ORIENTED_EDGE('',*,*,#3253,.T.);
#4663=ORIENTED_EDGE('',*,*,#3251,.T.);
#4664=ORIENTED_EDGE('',*,*,#3253,.F.);
#4665=ORIENTED_EDGE('',*,*,#3254,.F.);
#4666=ORIENTED_EDGE('',*,*,#3255,.T.);
#4667=ORIENTED_EDGE('',*,*,#3252,.T.);
#4668=ORIENTED_EDGE('',*,*,#3255,.F.);
#4669=ORIENTED_EDGE('',*,*,#3256,.F.);
#4670=ORIENTED_EDGE('',*,*,#3254,.T.);
#4671=ORIENTED_EDGE('',*,*,#3248,.F.);
#4672=ORIENTED_EDGE('',*,*,#3257,.T.);
#4673=ORIENTED_EDGE('',*,*,#3256,.T.);
#4674=ORIENTED_EDGE('',*,*,#3257,.F.);
#4873=PLANE('',#5757);
#4874=PLANE('',#5762);
#4875=PLANE('',#5768);
#5132=ADVANCED_FACE('',(#559,#300),#4873,.T.);
#5133=ADVANCED_FACE('',(#560),#232,.T.);
#5134=ADVANCED_FACE('',(#561,#301),#4874,.T.);
#5135=ADVANCED_FACE('',(#562),#105,.F.);
#5136=ADVANCED_FACE('',(#563),#233,.F.);
#5137=ADVANCED_FACE('',(#564,#302),#4875,.T.);
#5138=ADVANCED_FACE('',(#565),#106,.T.);
#5156=CLOSED_SHELL('',(#5132,#5133,#5134,#5135,#5136,#5137,#5138));
#5756=AXIS2_PLACEMENT_3D('',#8832,#7256,#7257);
#5757=AXIS2_PLACEMENT_3D('',#8833,#7258,#7259);
#5758=AXIS2_PLACEMENT_3D('',#8835,#7260,#7261);
#5759=AXIS2_PLACEMENT_3D('',#8837,#7262,#7263);
#5760=AXIS2_PLACEMENT_3D('',#8838,#7264,#7265);
#5761=AXIS2_PLACEMENT_3D('',#8840,#7266,#7267);
#5762=AXIS2_PLACEMENT_3D('',#8842,#7269,#7270);
#5763=AXIS2_PLACEMENT_3D('',#8844,#7271,#7272);
#5764=AXIS2_PLACEMENT_3D('',#8845,#7273,#7274);
#5765=AXIS2_PLACEMENT_3D('',#8847,#7275,#7276);
#5766=AXIS2_PLACEMENT_3D('',#8849,#7278,#7279);
#5767=AXIS2_PLACEMENT_3D('',#8851,#7280,#7281);
#5768=AXIS2_PLACEMENT_3D('',#8853,#7283,#7284);
#5769=AXIS2_PLACEMENT_3D('',#8855,#7285,#7286);
#5770=AXIS2_PLACEMENT_3D('',#8856,#7287,#7288);
#7256=DIRECTION('axis',(0.,0.,1.));
#7257=DIRECTION('refdir',(1.,0.,0.));
#7258=DIRECTION('center_axis',(0.,-1.,0.));
#7259=DIRECTION('ref_axis',(0.,0.,-1.));
#7260=DIRECTION('center_axis',(0.,1.,0.));
#7261=DIRECTION('ref_axis',(1.,0.,0.));
#7262=DIRECTION('center_axis',(0.,1.,0.));
#7263=DIRECTION('ref_axis',(1.,0.,0.));
#7264=DIRECTION('center_axis',(0.,1.,0.));
#7265=DIRECTION('ref_axis',(0.,0.,1.));
#7266=DIRECTION('center_axis',(0.,1.,0.));
#7267=DIRECTION('ref_axis',(1.,0.,0.));
#7268=DIRECTION('',(0.,-1.,0.));
#7269=DIRECTION('center_axis',(0.,1.,0.));
#7270=DIRECTION('ref_axis',(1.,0.,0.));
#7271=DIRECTION('center_axis',(0.,1.,0.));
#7272=DIRECTION('ref_axis',(1.,0.,0.));
#7273=DIRECTION('center_axis',(0.,1.,0.));
#7274=DIRECTION('ref_axis',(0.,0.,1.));
#7275=DIRECTION('center_axis',(0.,1.,0.));
#7276=DIRECTION('ref_axis',(1.,0.,0.));
#7277=DIRECTION('',(-8.65956056235493E-17,0.707106781186548,-0.707106781186547));
#7278=DIRECTION('center_axis',(0.,1.,0.));
#7279=DIRECTION('ref_axis',(0.,0.,1.));
#7280=DIRECTION('center_axis',(0.,1.,0.));
#7281=DIRECTION('ref_axis',(1.,0.,0.));
#7282=DIRECTION('',(0.,1.,0.));
#7283=DIRECTION('center_axis',(0.,-1.,0.));
#7284=DIRECTION('ref_axis',(0.,0.,-1.));
#7285=DIRECTION('center_axis',(0.,1.,0.));
#7286=DIRECTION('ref_axis',(1.,0.,0.));
#7287=DIRECTION('center_axis',(0.,1.,0.));
#7288=DIRECTION('ref_axis',(0.,0.,1.));
#7289=DIRECTION('',(8.65956056235493E-17,-0.707106781186548,0.707106781186547));
#8832=CARTESIAN_POINT('',(0.,0.,0.));
#8833=CARTESIAN_POINT('Origin',(0.,-0.0116999997384846,0.0065));
#8834=CARTESIAN_POINT('',(-7.9602041944578E-19,-0.0116999997384946,-0.0065));
#8835=CARTESIAN_POINT('Origin',(0.,-0.0116999997384946,0.));
#8836=CARTESIAN_POINT('',(-5.87830450451699E-19,-0.0116999997384846,-0.00479999989271167));
#8837=CARTESIAN_POINT('Origin',(0.,-0.0116999997384946,0.));
#8838=CARTESIAN_POINT('Origin',(0.,-0.0113499997351319,0.));
#8839=CARTESIAN_POINT('',(-7.9602041944578E-19,-0.0109999997317891,-0.0065));
#8840=CARTESIAN_POINT('Origin',(0.,-0.0109999997317891,0.));
#8841=CARTESIAN_POINT('',(-7.9602041944578E-19,-0.0113499997351319,-0.0065));
#8842=CARTESIAN_POINT('Origin',(0.,-0.0109999997317791,0.00455));
#8843=CARTESIAN_POINT('',(-5.57214293612046E-19,-0.0109999997317791,-0.00455));
#8844=CARTESIAN_POINT('Origin',(0.,-0.0109999997317891,0.));
#8845=CARTESIAN_POINT('Origin',(0.,-0.0112499997317791,0.));
#8846=CARTESIAN_POINT('',(-4.95981953654678E-19,-0.0114999997317791,-0.00405));
#8847=CARTESIAN_POINT('Origin',(0.,-0.0114999997317891,0.));
#8848=CARTESIAN_POINT('',(-5.26598123633362E-19,-0.0112499997317791,-0.0043));
#8849=CARTESIAN_POINT('Origin',(0.,-0.0117499997317791,0.));
#8850=CARTESIAN_POINT('',(-4.95981953654678E-19,-0.0119999997317891,-0.00405));
#8851=CARTESIAN_POINT('Origin',(0.,-0.0119999997317891,0.));
#8852=CARTESIAN_POINT('',(-4.95981953654678E-19,-0.0117499997317791,-0.00405));
#8853=CARTESIAN_POINT('Origin',(0.,-0.0119999997317791,0.00449999989941716));
#8854=CARTESIAN_POINT('',(-5.51091047298466E-19,-0.0119999997317791,-0.00449999989941718));
#8855=CARTESIAN_POINT('Origin',(0.,-0.0119999997317891,0.));
#8856=CARTESIAN_POINT('Origin',(0.,-0.0118499997351319,0.));
#8857=CARTESIAN_POINT('',(-5.69460748875079E-19,-0.0118499997351319,-0.0046499998960644));
#8929=UNCERTAINTY_MEASURE_WITH_UNIT(LENGTH_MEASURE(1.E-5),#8945,
'DISTANCE_ACCURACY_VALUE',
'Maximum model space distance between geometric entities at asserted c
onnectivities');
#8932=UNCERTAINTY_MEASURE_WITH_UNIT(LENGTH_MEASURE(1.E-5),#8945,
'DISTANCE_ACCURACY_VALUE',
'Maximum model space distance between geometric entities at asserted c
onnectivities');
#8941=(
GEOMETRIC_REPRESENTATION_CONTEXT(3)
GLOBAL_UNCERTAINTY_ASSIGNED_CONTEXT((#8929))
GLOBAL_UNIT_ASSIGNED_CONTEXT((#8945,#8946,#8947))
REPRESENTATION_CONTEXT('','3D')
);
#8944=(
GEOMETRIC_REPRESENTATION_CONTEXT(3)
GLOBAL_UNCERTAINTY_ASSIGNED_CONTEXT((#8932))
GLOBAL_UNIT_ASSIGNED_CONTEXT((#8945,#8946,#8947))
REPRESENTATION_CONTEXT('','3D')
);
#8945=(
LENGTH_UNIT()
NAMED_UNIT(*)
SI_UNIT($,.METRE.)
);
#8946=(
NAMED_UNIT(*)
PLANE_ANGLE_UNIT()
SI_UNIT($,.RADIAN.)
);
#8947=(
NAMED_UNIT(*)
SI_UNIT($,.STERADIAN.)
SOLID_ANGLE_UNIT()
);
#8956=SHAPE_DEFINITION_REPRESENTATION(#8967,#9000);
#8967=PRODUCT_DEFINITION_SHAPE('',$,#9012);
#9000=SHAPE_REPRESENTATION('',(#5756),#8941);
#9003=PRODUCT_DEFINITION_CONTEXT('part definition',#9038,'design');
#9012=PRODUCT_DEFINITION('Bearing Retainer','Bearing Retainer 1',#9023,
#9003);
#9023=PRODUCT_DEFINITION_FORMATION('',$,#9048);
#9038=APPLICATION_CONTEXT('Managed model based 3d engineering');
#9039=PRODUCT_CONTEXT('part definition',#9038,'mechanical');
#9048=PRODUCT('Bearing Retainer','Bearing Retainer 1',
'LEGAL AND USAGE DISCLAIMER: this Data/Model is provided \X2\201C\X0\A
S IS\X2\201D\X0\ for informational and representational only. It is a 
geometric approximation and is NOT engineered, certified, or guarantee
d for dimensional accuracy, exact tolerances, or production-level prec
ision. Vendor disclaims all implied warranties including fitness for a
 particular purpose. DO NOT USE FOR DIRECT PHYSICAL MANUFACTURING, AUT
OMATED PRODUCTION, OR SAFETY-CRITICAL SYSTEMS without independent engi
neering verification and resolution of any design discrepancies.',(#9039));
#9052=PRESENTATION_STYLE_ASSIGNMENT((#9057));
#9057=SURFACE_STYLE_USAGE(.BOTH.,#9062);
#9062=SURFACE_SIDE_STYLE('',(#9067));
#9067=SURFACE_STYLE_FILL_AREA(#9072);
#9072=FILL_AREA_STYLE('Opaque(25,25,25)',(#9077));
#9077=FILL_AREA_STYLE_COLOUR('Opaque(25,25,25)',#9082);
#9082=COLOUR_RGB('Opaque(25,25,25)',0.0980392156862745,0.0980392156862745,
0.0980392156862745);
ENDSEC;
END-ISO-10303-21;
